ISO-10303-21;
HEADER;
/* Generated by software containing ST-Developer
 * from STEP Tools, Inc. (www.steptools.com) 
 */

FILE_DESCRIPTION(
/* description */ ('Bearing friction torque test rig'),
/* implementation_level */ '2;1');

FILE_NAME(
/* name */ 'Support housing (1).step',
/* time_stamp */ '2026-10-28T03:24:04-07:00',
/* author */ (''),
/* organization */ (''),
/* preprocessor_version */ 'ST-DEVELOPER v20.2',
/* originating_system */ 'Autodesk Translation Framework v15.17.0.0',
/* authorisation */ '');

FILE_SCHEMA (('AUTOMOTIVE_DESIGN { 1 0 10303 214 3 1 1 }'));
ENDSEC;

DATA;
#10=MECHANICAL_DESIGN_GEOMETRIC_PRESENTATION_REPRESENTATION('',(#543),#14822);
#458=ELLIPSE('',#8300,1.22383731671239,0.6);
#459=ELLIPSE('',#8301,1.22383731671239,0.6);
#460=ELLIPSE('',#8309,1.22383731671239,0.6);
#465=SHAPE_REPRESENTATION_RELATIONSHIP('SRR','None',#15004,#504);
#504=ADVANCED_BREP_SHAPE_REPRESENTATION('',(#597),#14784);
#543=STYLED_ITEM('',(#15263),#597);
#597=MANIFOLD_SOLID_BREP('Body1',#7659);
#706=FACE_BOUND('',#1672,.T.);
#707=FACE_BOUND('',#1676,.T.);
#708=FACE_BOUND('',#1680,.T.);
#709=FACE_BOUND('',#1682,.T.);
#710=FACE_BOUND('',#1685,.T.);
#711=FACE_BOUND('',#1686,.T.);
#712=FACE_BOUND('',#1689,.T.);
#713=FACE_BOUND('',#1690,.T.);
#714=FACE_BOUND('',#1691,.T.);
#715=FACE_BOUND('',#1692,.T.);
#716=FACE_BOUND('',#1693,.T.);
#717=FACE_BOUND('',#1697,.T.);
#718=FACE_BOUND('',#1698,.T.);
#719=FACE_BOUND('',#1699,.T.);
#720=FACE_BOUND('',#1700,.T.);
#721=FACE_BOUND('',#1701,.T.);
#897=PLANE('',#8296);
#898=PLANE('',#8302);
#899=PLANE('',#8304);
#900=PLANE('',#8310);
#901=PLANE('',#8316);
#902=PLANE('',#8317);
#903=PLANE('',#8318);
#904=PLANE('',#8319);
#905=PLANE('',#8320);
#906=PLANE('',#8321);
#907=PLANE('',#8328);
#1158=FACE_OUTER_BOUND('',#1665,.T.);
#1159=FACE_OUTER_BOUND('',#1666,.T.);
#1160=FACE_OUTER_BOUND('',#1667,.T.);
#1161=FACE_OUTER_BOUND('',#1668,.T.);
#1162=FACE_OUTER_BOUND('',#1669,.T.);
#1163=FACE_OUTER_BOUND('',#1670,.T.);
#1164=FACE_OUTER_BOUND('',#1671,.T.);
#1165=FACE_OUTER_BOUND('',#1673,.T.);
#1166=FACE_OUTER_BOUND('',#1674,.T.);
#1167=FACE_OUTER_BOUND('',#1675,.T.);
#1168=FACE_OUTER_BOUND('',#1677,.T.);
#1169=FACE_OUTER_BOUND('',#1678,.T.);
#1170=FACE_OUTER_BOUND('',#1679,.T.);
#1171=FACE_OUTER_BOUND('',#1681,.T.);
#1172=FACE_OUTER_BOUND('',#1683,.T.);
#1173=FACE_OUTER_BOUND('',#1684,.T.);
#1174=FACE_OUTER_BOUND('',#1687,.T.);
#1175=FACE_OUTER_BOUND('',#1688,.T.);
#1176=FACE_OUTER_BOUND('',#1694,.T.);
#1177=FACE_OUTER_BOUND('',#1695,.T.);
#1178=FACE_OUTER_BOUND('',#1696,.T.);
#1665=EDGE_LOOP('',(#5430,#5431,#5432,#5433));
#1666=EDGE_LOOP('',(#5434,#5435,#5436,#5437));
#1667=EDGE_LOOP('',(#5438,#5439,#5440,#5441));
#1668=EDGE_LOOP('',(#5442,#5443,#5444,#5445));
#1669=EDGE_LOOP('',(#5446,#5447));
#1670=EDGE_LOOP('',(#5448,#5449,#5450,#5451,#5452,#5453));
#1671=EDGE_LOOP('',(#5454));
#1672=EDGE_LOOP('',(#5455));
#1673=EDGE_LOOP('',(#5456,#5457,#5458));
#1674=EDGE_LOOP('',(#5459,#5460,#5461,#5462,#5463,#5464));
#1675=EDGE_LOOP('',(#5465));
#1676=EDGE_LOOP('',(#5466));
#1677=EDGE_LOOP('',(#5467,#5468,#5469,#5470));
#1678=EDGE_LOOP('',(#5471,#5472,#5473,#5474));
#1679=EDGE_LOOP('',(#5475,#5476,#5477,#5478));
#1680=EDGE_LOOP('',(#5479,#5480));
#1681=EDGE_LOOP('',(#5481,#5482,#5483,#5484));
#1682=EDGE_LOOP('',(#5485,#5486,#5487));
#1683=EDGE_LOOP('',(#5488,#5489,#5490,#5491));
#1684=EDGE_LOOP('',(#5492,#5493,#5494,#5495));
#1685=EDGE_LOOP('',(#5496));
#1686=EDGE_LOOP('',(#5497));
#1687=EDGE_LOOP('',(#5498,#5499,#5500,#5501));
#1688=EDGE_LOOP('',(#5502,#5503,#5504,#5505,#5506,#5507));
#1689=EDGE_LOOP('',(#5508));
#1690=EDGE_LOOP('',(#5509));
#1691=EDGE_LOOP('',(#5510));
#1692=EDGE_LOOP('',(#5511));
#1693=EDGE_LOOP('',(#5512));
#1694=EDGE_LOOP('',(#5513,#5514,#5515,#5516));
#1695=EDGE_LOOP('',(#5517,#5518,#5519,#5520));
#1696=EDGE_LOOP('',(#5521,#5522,#5523,#5524,#5525,#5526));
#1697=EDGE_LOOP('',(#5527));
#1698=EDGE_LOOP('',(#5528));
#1699=EDGE_LOOP('',(#5529));
#1700=EDGE_LOOP('',(#5530));
#1701=EDGE_LOOP('',(#5531));
#2284=LINE('',#11963,#2728);
#2285=LINE('',#11969,#2729);
#2286=LINE('',#11975,#2730);
#2287=LINE('',#11981,#2731);
#2288=LINE('',#11986,#2732);
#2289=LINE('',#11992,#2733);
#2290=LINE('',#12001,#2734);
#2291=LINE('',#12008,#2735);
#2292=LINE('',#12016,#2736);
#2293=LINE('',#12020,#2737);
#2294=LINE('',#12024,#2738);
#2295=LINE('',#12026,#2739);
#2296=LINE('',#12028,#2740);
#2297=LINE('',#12029,#2741);
#2298=LINE('',#12033,#2742);
#2299=LINE('',#12035,#2743);
#2300=LINE('',#12037,#2744);
#2301=LINE('',#12038,#2745);
#2302=LINE('',#12041,#2746);
#2303=LINE('',#12043,#2747);
#2304=LINE('',#12044,#2748);
#2305=LINE('',#12047,#2749);
#2306=LINE('',#12049,#2750);
#2307=LINE('',#12050,#2751);
#2308=LINE('',#12052,#2752);
#2309=LINE('',#12053,#2753);
#2310=LINE('',#12060,#2754);
#2728=VECTOR('',#9519,0.165);
#2729=VECTOR('',#9526,0.165);
#2730=VECTOR('',#9533,0.165);
#2731=VECTOR('',#9540,0.165);
#2732=VECTOR('',#9545,1.);
#2733=VECTOR('',#9552,0.6);
#2734=VECTOR('',#9563,1.);
#2735=VECTOR('',#9572,0.6);
#2736=VECTOR('',#9583,0.33);
#2737=VECTOR('',#9588,0.33);
#2738=VECTOR('',#9591,1.);
#2739=VECTOR('',#9592,1.);
#2740=VECTOR('',#9593,1.);
#2741=VECTOR('',#9594,1.);
#2742=VECTOR('',#9597,1.);
#2743=VECTOR('',#9598,1.);
#2744=VECTOR('',#9599,1.);
#2745=VECTOR('',#9600,1.);
#2746=VECTOR('',#9603,1.);
#2747=VECTOR('',#9604,1.);
#2748=VECTOR('',#9605,1.);
#2749=VECTOR('',#9608,1.);
#2750=VECTOR('',#9609,1.);
#2751=VECTOR('',#9610,1.);
#2752=VECTOR('',#9613,1.);
#2753=VECTOR('',#9614,1.);
#2754=VECTOR('',#9623,1.6);
#3180=CIRCLE('',#8285,0.165);
#3181=CIRCLE('',#8286,0.165);
#3182=CIRCLE('',#8288,0.165);
#3183=CIRCLE('',#8289,0.165);
#3184=CIRCLE('',#8291,0.165);
#3185=CIRCLE('',#8292,0.165);
#3186=CIRCLE('',#8294,0.165);
#3187=CIRCLE('',#8295,0.165);
#3188=CIRCLE('',#8297,0.6);
#3189=CIRCLE('',#8299,0.6);
#3190=CIRCLE('',#8303,0.33);
#3191=CIRCLE('',#8305,0.6);
#3192=CIRCLE('',#8306,0.6);
#3193=CIRCLE('',#8308,0.6);
#3194=CIRCLE('',#8311,0.33);
#3195=CIRCLE('',#8313,0.33);
#3196=CIRCLE('',#8315,0.33);
#3197=CIRCLE('',#8322,2.5);
#3198=CIRCLE('',#8323,1.6);
#3199=CIRCLE('',#8325,1.6);
#3200=CIRCLE('',#8327,2.5);
#3647=VERTEX_POINT('',#11960);
#3648=VERTEX_POINT('',#11962);
#3649=VERTEX_POINT('',#11966);
#3650=VERTEX_POINT('',#11968);
#3651=VERTEX_POINT('',#11972);
#3652=VERTEX_POINT('',#11974);
#3653=VERTEX_POINT('',#11978);
#3654=VERTEX_POINT('',#11980);
#3655=VERTEX_POINT('',#11984);
#3656=VERTEX_POINT('',#11985);
#3657=VERTEX_POINT('',#11989);
#3658=VERTEX_POINT('',#11991);
#3659=VERTEX_POINT('',#11996);
#3660=VERTEX_POINT('',#11999);
#3661=VERTEX_POINT('',#12000);
#3662=VERTEX_POINT('',#12002);
#3663=VERTEX_POINT('',#12006);
#3664=VERTEX_POINT('',#12011);
#3665=VERTEX_POINT('',#12014);
#3666=VERTEX_POINT('',#12018);
#3667=VERTEX_POINT('',#12022);
#3668=VERTEX_POINT('',#12023);
#3669=VERTEX_POINT('',#12025);
#3670=VERTEX_POINT('',#12027);
#3671=VERTEX_POINT('',#12031);
#3672=VERTEX_POINT('',#12032);
#3673=VERTEX_POINT('',#12034);
#3674=VERTEX_POINT('',#12036);
#3675=VERTEX_POINT('',#12040);
#3676=VERTEX_POINT('',#12042);
#3677=VERTEX_POINT('',#12046);
#3678=VERTEX_POINT('',#12048);
#3679=VERTEX_POINT('',#12056);
#3680=VERTEX_POINT('',#12059);
#4341=EDGE_CURVE('',#3647,#3647,#3180,.T.);
#4342=EDGE_CURVE('',#3647,#3648,#2284,.T.);
#4343=EDGE_CURVE('',#3648,#3648,#3181,.T.);
#4344=EDGE_CURVE('',#3649,#3649,#3182,.T.);
#4345=EDGE_CURVE('',#3649,#3650,#2285,.T.);
#4346=EDGE_CURVE('',#3650,#3650,#3183,.T.);
#4347=EDGE_CURVE('',#3651,#3651,#3184,.T.);
#4348=EDGE_CURVE('',#3651,#3652,#2286,.T.);
#4349=EDGE_CURVE('',#3652,#3652,#3185,.T.);
#4350=EDGE_CURVE('',#3653,#3653,#3186,.T.);
#4351=EDGE_CURVE('',#3653,#3654,#2287,.T.);
#4352=EDGE_CURVE('',#3654,#3654,#3187,.T.);
#4353=EDGE_CURVE('',#3655,#3656,#2288,.T.);
#4354=EDGE_CURVE('',#3656,#3655,#3188,.T.);
#4355=EDGE_CURVE('',#3657,#3657,#3189,.T.);
#4356=EDGE_CURVE('',#3657,#3658,#2289,.T.);
#4357=EDGE_CURVE('',#3656,#3658,#458,.T.);
#4358=EDGE_CURVE('',#3658,#3655,#459,.T.);
#4359=EDGE_CURVE('',#3659,#3659,#3190,.T.);
#4360=EDGE_CURVE('',#3660,#3661,#2290,.T.);
#4361=EDGE_CURVE('',#3662,#3660,#3191,.T.);
#4362=EDGE_CURVE('',#3661,#3662,#3192,.T.);
#4363=EDGE_CURVE('',#3663,#3663,#3193,.T.);
#4364=EDGE_CURVE('',#3663,#3662,#2291,.T.);
#4365=EDGE_CURVE('',#3661,#3660,#460,.T.);
#4366=EDGE_CURVE('',#3664,#3664,#3194,.T.);
#4367=EDGE_CURVE('',#3665,#3665,#3195,.T.);
#4368=EDGE_CURVE('',#3665,#3659,#2292,.T.);
#4369=EDGE_CURVE('',#3666,#3666,#3196,.T.);
#4370=EDGE_CURVE('',#3666,#3664,#2293,.T.);
#4371=EDGE_CURVE('',#3667,#3668,#2294,.T.);
#4372=EDGE_CURVE('',#3669,#3667,#2295,.T.);
#4373=EDGE_CURVE('',#3669,#3670,#2296,.T.);
#4374=EDGE_CURVE('',#3668,#3670,#2297,.T.);
#4375=EDGE_CURVE('',#3671,#3672,#2298,.T.);
#4376=EDGE_CURVE('',#3673,#3671,#2299,.T.);
#4377=EDGE_CURVE('',#3674,#3673,#2300,.T.);
#4378=EDGE_CURVE('',#3672,#3674,#2301,.T.);
#4379=EDGE_CURVE('',#3674,#3675,#2302,.T.);
#4380=EDGE_CURVE('',#3676,#3673,#2303,.T.);
#4381=EDGE_CURVE('',#3675,#3676,#2304,.T.);
#4382=EDGE_CURVE('',#3675,#3677,#2305,.T.);
#4383=EDGE_CURVE('',#3678,#3676,#2306,.T.);
#4384=EDGE_CURVE('',#3677,#3678,#2307,.T.);
#4385=EDGE_CURVE('',#3677,#3669,#2308,.T.);
#4386=EDGE_CURVE('',#3670,#3678,#2309,.T.);
#4387=EDGE_CURVE('',#3671,#3668,#3197,.T.);
#4388=EDGE_CURVE('',#3679,#3679,#3198,.T.);
#4389=EDGE_CURVE('',#3679,#3680,#2310,.T.);
#4390=EDGE_CURVE('',#3680,#3680,#3199,.T.);
#4391=EDGE_CURVE('',#3672,#3667,#3200,.T.);
#5430=ORIENTED_EDGE('',*,*,#4341,.F.);
#5431=ORIENTED_EDGE('',*,*,#4342,.T.);
#5432=ORIENTED_EDGE('',*,*,#4343,.F.);
#5433=ORIENTED_EDGE('',*,*,#4342,.F.);
#5434=ORIENTED_EDGE('',*,*,#4344,.F.);
#5435=ORIENTED_EDGE('',*,*,#4345,.T.);
#5436=ORIENTED_EDGE('',*,*,#4346,.F.);
#5437=ORIENTED_EDGE('',*,*,#4345,.F.);
#5438=ORIENTED_EDGE('',*,*,#4347,.F.);
#5439=ORIENTED_EDGE('',*,*,#4348,.T.);
#5440=ORIENTED_EDGE('',*,*,#4349,.F.);
#5441=ORIENTED_EDGE('',*,*,#4348,.F.);
#5442=ORIENTED_EDGE('',*,*,#4350,.F.);
#5443=ORIENTED_EDGE('',*,*,#4351,.T.);
#5444=ORIENTED_EDGE('',*,*,#4352,.F.);
#5445=ORIENTED_EDGE('',*,*,#4351,.F.);
#5446=ORIENTED_EDGE('',*,*,#4353,.F.);
#5447=ORIENTED_EDGE('',*,*,#4354,.F.);
#5448=ORIENTED_EDGE('',*,*,#4355,.F.);
#5449=ORIENTED_EDGE('',*,*,#4356,.T.);
#5450=ORIENTED_EDGE('',*,*,#4357,.F.);
#5451=ORIENTED_EDGE('',*,*,#4354,.T.);
#5452=ORIENTED_EDGE('',*,*,#4358,.F.);
#5453=ORIENTED_EDGE('',*,*,#4356,.F.);
#5454=ORIENTED_EDGE('',*,*,#4355,.T.);
#5455=ORIENTED_EDGE('',*,*,#4359,.F.);
#5456=ORIENTED_EDGE('',*,*,#4360,.F.);
#5457=ORIENTED_EDGE('',*,*,#4361,.F.);
#5458=ORIENTED_EDGE('',*,*,#4362,.F.);
#5459=ORIENTED_EDGE('',*,*,#4363,.F.);
#5460=ORIENTED_EDGE('',*,*,#4364,.T.);
#5461=ORIENTED_EDGE('',*,*,#4361,.T.);
#5462=ORIENTED_EDGE('',*,*,#4365,.F.);
#5463=ORIENTED_EDGE('',*,*,#4362,.T.);
#5464=ORIENTED_EDGE('',*,*,#4364,.F.);
#5465=ORIENTED_EDGE('',*,*,#4363,.T.);
#5466=ORIENTED_EDGE('',*,*,#4366,.F.);
#5467=ORIENTED_EDGE('',*,*,#4367,.F.);
#5468=ORIENTED_EDGE('',*,*,#4368,.T.);
#5469=ORIENTED_EDGE('',*,*,#4359,.T.);
#5470=ORIENTED_EDGE('',*,*,#4368,.F.);
#5471=ORIENTED_EDGE('',*,*,#4369,.F.);
#5472=ORIENTED_EDGE('',*,*,#4370,.T.);
#5473=ORIENTED_EDGE('',*,*,#4366,.T.);
#5474=ORIENTED_EDGE('',*,*,#4370,.F.);
#5475=ORIENTED_EDGE('',*,*,#4371,.F.);
#5476=ORIENTED_EDGE('',*,*,#4372,.F.);
#5477=ORIENTED_EDGE('',*,*,#4373,.T.);
#5478=ORIENTED_EDGE('',*,*,#4374,.F.);
#5479=ORIENTED_EDGE('',*,*,#4365,.T.);
#5480=ORIENTED_EDGE('',*,*,#4360,.T.);
#5481=ORIENTED_EDGE('',*,*,#4375,.F.);
#5482=ORIENTED_EDGE('',*,*,#4376,.F.);
#5483=ORIENTED_EDGE('',*,*,#4377,.F.);
#5484=ORIENTED_EDGE('',*,*,#4378,.F.);
#5485=ORIENTED_EDGE('',*,*,#4357,.T.);
#5486=ORIENTED_EDGE('',*,*,#4358,.T.);
#5487=ORIENTED_EDGE('',*,*,#4353,.T.);
#5488=ORIENTED_EDGE('',*,*,#4379,.F.);
#5489=ORIENTED_EDGE('',*,*,#4377,.T.);
#5490=ORIENTED_EDGE('',*,*,#4380,.F.);
#5491=ORIENTED_EDGE('',*,*,#4381,.F.);
#5492=ORIENTED_EDGE('',*,*,#4382,.F.);
#5493=ORIENTED_EDGE('',*,*,#4381,.T.);
#5494=ORIENTED_EDGE('',*,*,#4383,.F.);
#5495=ORIENTED_EDGE('',*,*,#4384,.F.);
#5496=ORIENTED_EDGE('',*,*,#4367,.T.);
#5497=ORIENTED_EDGE('',*,*,#4369,.T.);
#5498=ORIENTED_EDGE('',*,*,#4385,.F.);
#5499=ORIENTED_EDGE('',*,*,#4384,.T.);
#5500=ORIENTED_EDGE('',*,*,#4386,.F.);
#5501=ORIENTED_EDGE('',*,*,#4373,.F.);
#5502=ORIENTED_EDGE('',*,*,#4387,.T.);
#5503=ORIENTED_EDGE('',*,*,#4374,.T.);
#5504=ORIENTED_EDGE('',*,*,#4386,.T.);
#5505=ORIENTED_EDGE('',*,*,#4383,.T.);
#5506=ORIENTED_EDGE('',*,*,#4380,.T.);
#5507=ORIENTED_EDGE('',*,*,#4376,.T.);
#5508=ORIENTED_EDGE('',*,*,#4388,.T.);
#5509=ORIENTED_EDGE('',*,*,#4352,.T.);
#5510=ORIENTED_EDGE('',*,*,#4349,.T.);
#5511=ORIENTED_EDGE('',*,*,#4346,.T.);
#5512=ORIENTED_EDGE('',*,*,#4343,.T.);
#5513=ORIENTED_EDGE('',*,*,#4388,.F.);
#5514=ORIENTED_EDGE('',*,*,#4389,.T.);
#5515=ORIENTED_EDGE('',*,*,#4390,.T.);
#5516=ORIENTED_EDGE('',*,*,#4389,.F.);
#5517=ORIENTED_EDGE('',*,*,#4371,.T.);
#5518=ORIENTED_EDGE('',*,*,#4387,.F.);
#5519=ORIENTED_EDGE('',*,*,#4375,.T.);
#5520=ORIENTED_EDGE('',*,*,#4391,.T.);
#5521=ORIENTED_EDGE('',*,*,#4391,.F.);
#5522=ORIENTED_EDGE('',*,*,#4378,.T.);
#5523=ORIENTED_EDGE('',*,*,#4379,.T.);
#5524=ORIENTED_EDGE('',*,*,#4382,.T.);
#5525=ORIENTED_EDGE('',*,*,#4385,.T.);
#5526=ORIENTED_EDGE('',*,*,#4372,.T.);
#5527=ORIENTED_EDGE('',*,*,#4390,.F.);
#5528=ORIENTED_EDGE('',*,*,#4350,.T.);
#5529=ORIENTED_EDGE('',*,*,#4347,.T.);
#5530=ORIENTED_EDGE('',*,*,#4344,.T.);
#5531=ORIENTED_EDGE('',*,*,#4341,.T.);
#7080=CYLINDRICAL_SURFACE('',#8284,0.165);
#7081=CYLINDRICAL_SURFACE('',#8287,0.165);
#7082=CYLINDRICAL_SURFACE('',#8290,0.165);
#7083=CYLINDRICAL_SURFACE('',#8293,0.165);
#7084=CYLINDRICAL_SURFACE('',#8298,0.6);
#7085=CYLINDRICAL_SURFACE('',#8307,0.6);
#7086=CYLINDRICAL_SURFACE('',#8312,0.33);
#7087=CYLINDRICAL_SURFACE('',#8314,0.33);
#7088=CYLINDRICAL_SURFACE('',#8324,1.6);
#7089=CYLINDRICAL_SURFACE('',#8326,2.5);
#7269=ADVANCED_FACE('',(#1158),#7080,.F.);
#7270=ADVANCED_FACE('',(#1159),#7081,.F.);
#7271=ADVANCED_FACE('',(#1160),#7082,.F.);
#7272=ADVANCED_FACE('',(#1161),#7083,.F.);
#7273=ADVANCED_FACE('',(#1162),#897,.F.);
#7274=ADVANCED_FACE('',(#1163),#7084,.F.);
#7275=ADVANCED_FACE('',(#1164,#706),#898,.T.);
#7276=ADVANCED_FACE('',(#1165),#899,.F.);
#7277=ADVANCED_FACE('',(#1166),#7085,.F.);
#7278=ADVANCED_FACE('',(#1167,#707),#900,.T.);
#7279=ADVANCED_FACE('',(#1168),#7086,.F.);
#7280=ADVANCED_FACE('',(#1169),#7087,.F.);
#7281=ADVANCED_FACE('',(#1170,#708),#901,.T.);
#7282=ADVANCED_FACE('',(#1171,#709),#902,.T.);
#7283=ADVANCED_FACE('',(#1172),#903,.T.);
#7284=ADVANCED_FACE('',(#1173,#710,#711),#904,.T.);
#7285=ADVANCED_FACE('',(#1174),#905,.T.);
#7286=ADVANCED_FACE('',(#1175,#712,#713,#714,#715,#716),#906,.T.);
#7287=ADVANCED_FACE('',(#1176),#7088,.F.);
#7288=ADVANCED_FACE('',(#1177),#7089,.T.);
#7289=ADVANCED_FACE('',(#1178,#717,#718,#719,#720,#721),#907,.F.);
#7659=CLOSED_SHELL('',(#7269,#7270,#7271,#7272,#7273,#7274,#7275,#7276,
#7277,#7278,#7279,#7280,#7281,#7282,#7283,#7284,#7285,#7286,#7287,#7288,
#7289));
#8283=AXIS2_PLACEMENT_3D('',#11958,#9513,#9514);
#8284=AXIS2_PLACEMENT_3D('',#11959,#9515,#9516);
#8285=AXIS2_PLACEMENT_3D('',#11961,#9517,#9518);
#8286=AXIS2_PLACEMENT_3D('',#11964,#9520,#9521);
#8287=AXIS2_PLACEMENT_3D('',#11965,#9522,#9523);
#8288=AXIS2_PLACEMENT_3D('',#11967,#9524,#9525);
#8289=AXIS2_PLACEMENT_3D('',#11970,#9527,#9528);
#8290=AXIS2_PLACEMENT_3D('',#11971,#9529,#9530);
#8291=AXIS2_PLACEMENT_3D('',#11973,#9531,#9532);
#8292=AXIS2_PLACEMENT_3D('',#11976,#9534,#9535);
#8293=AXIS2_PLACEMENT_3D('',#11977,#9536,#9537);
#8294=AXIS2_PLACEMENT_3D('',#11979,#9538,#9539);
#8295=AXIS2_PLACEMENT_3D('',#11982,#9541,#9542);
#8296=AXIS2_PLACEMENT_3D('',#11983,#9543,#9544);
#8297=AXIS2_PLACEMENT_3D('',#11987,#9546,#9547);
#8298=AXIS2_PLACEMENT_3D('',#11988,#9548,#9549);
#8299=AXIS2_PLACEMENT_3D('',#11990,#9550,#9551);
#8300=AXIS2_PLACEMENT_3D('',#11993,#9553,#9554);
#8301=AXIS2_PLACEMENT_3D('',#11994,#9555,#9556);
#8302=AXIS2_PLACEMENT_3D('',#11995,#9557,#9558);
#8303=AXIS2_PLACEMENT_3D('',#11997,#9559,#9560);
#8304=AXIS2_PLACEMENT_3D('',#11998,#9561,#9562);
#8305=AXIS2_PLACEMENT_3D('',#12003,#9564,#9565);
#8306=AXIS2_PLACEMENT_3D('',#12004,#9566,#9567);
#8307=AXIS2_PLACEMENT_3D('',#12005,#9568,#9569);
#8308=AXIS2_PLACEMENT_3D('',#12007,#9570,#9571);
#8309=AXIS2_PLACEMENT_3D('',#12009,#9573,#9574);
#8310=AXIS2_PLACEMENT_3D('',#12010,#9575,#9576);
#8311=AXIS2_PLACEMENT_3D('',#12012,#9577,#9578);
#8312=AXIS2_PLACEMENT_3D('',#12013,#9579,#9580);
#8313=AXIS2_PLACEMENT_3D('',#12015,#9581,#9582);
#8314=AXIS2_PLACEMENT_3D('',#12017,#9584,#9585);
#8315=AXIS2_PLACEMENT_3D('',#12019,#9586,#9587);
#8316=AXIS2_PLACEMENT_3D('',#12021,#9589,#9590);
#8317=AXIS2_PLACEMENT_3D('',#12030,#9595,#9596);
#8318=AXIS2_PLACEMENT_3D('',#12039,#9601,#9602);
#8319=AXIS2_PLACEMENT_3D('',#12045,#9606,#9607);
#8320=AXIS2_PLACEMENT_3D('',#12051,#9611,#9612);
#8321=AXIS2_PLACEMENT_3D('',#12054,#9615,#9616);
#8322=AXIS2_PLACEMENT_3D('',#12055,#9617,#9618);
#8323=AXIS2_PLACEMENT_3D('',#12057,#9619,#9620);
#8324=AXIS2_PLACEMENT_3D('',#12058,#9621,#9622);
#8325=AXIS2_PLACEMENT_3D('',#12061,#9624,#9625);
#8326=AXIS2_PLACEMENT_3D('',#12062,#9626,#9627);
#8327=AXIS2_PLACEMENT_3D('',#12063,#9628,#9629);
#8328=AXIS2_PLACEMENT_3D('',#12064,#9630,#9631);
#9513=DIRECTION('axis',(0.,0.,1.));
#9514=DIRECTION('refdir',(1.,0.,0.));
#9515=DIRECTION('center_axis',(0.,1.,0.));
#9516=DIRECTION('ref_axis',(1.,0.,0.));
#9517=DIRECTION('center_axis',(0.,1.,0.));
#9518=DIRECTION('ref_axis',(1.,0.,0.));
#9519=DIRECTION('',(0.,1.,0.));
#9520=DIRECTION('center_axis',(0.,-1.,0.));
#9521=DIRECTION('ref_axis',(1.,0.,0.));
#9522=DIRECTION('center_axis',(0.,1.,0.));
#9523=DIRECTION('ref_axis',(1.,0.,0.));
#9524=DIRECTION('center_axis',(0.,1.,0.));
#9525=DIRECTION('ref_axis',(1.,0.,0.));
#9526=DIRECTION('',(0.,1.,0.));
#9527=DIRECTION('center_axis',(0.,-1.,0.));
#9528=DIRECTION('ref_axis',(1.,0.,0.));
#9529=DIRECTION('center_axis',(0.,1.,0.));
#9530=DIRECTION('ref_axis',(1.,0.,0.));
#9531=DIRECTION('center_axis',(0.,1.,0.));
#9532=DIRECTION('ref_axis',(1.,0.,0.));
#9533=DIRECTION('',(0.,1.,0.));
#9534=DIRECTION('center_axis',(0.,-1.,0.));
#9535=DIRECTION('ref_axis',(1.,0.,0.));
#9536=DIRECTION('center_axis',(0.,1.,0.));
#9537=DIRECTION('ref_axis',(1.,0.,0.));
#9538=DIRECTION('center_axis',(0.,1.,0.));
#9539=DIRECTION('ref_axis',(1.,0.,0.));
#9540=DIRECTION('',(0.,1.,0.));
#9541=DIRECTION('center_axis',(0.,-1.,0.));
#9542=DIRECTION('ref_axis',(1.,0.,0.));
#9543=DIRECTION('center_axis',(0.,0.,1.));
#9544=DIRECTION('ref_axis',(1.,0.,0.));
#9545=DIRECTION('',(0.,-1.,0.));
#9546=DIRECTION('center_axis',(0.,0.,1.));
#9547=DIRECTION('ref_axis',(1.,0.,0.));
#9548=DIRECTION('center_axis',(0.,0.,1.));
#9549=DIRECTION('ref_axis',(1.,0.,0.));
#9550=DIRECTION('center_axis',(0.,0.,1.));
#9551=DIRECTION('ref_axis',(1.,0.,0.));
#9552=DIRECTION('',(0.,0.,1.));
#9553=DIRECTION('center_axis',(0.871575537124549,0.,-0.490261239632559));
#9554=DIRECTION('ref_axis',(0.490261239632559,0.,0.871575537124549));
#9555=DIRECTION('center_axis',(0.871575537124549,0.,-0.490261239632559));
#9556=DIRECTION('ref_axis',(0.490261239632559,0.,0.871575537124549));
#9557=DIRECTION('center_axis',(0.,0.,1.));
#9558=DIRECTION('ref_axis',(1.,0.,0.));
#9559=DIRECTION('center_axis',(0.,0.,1.));
#9560=DIRECTION('ref_axis',(1.,0.,0.));
#9561=DIRECTION('center_axis',(0.,0.,1.));
#9562=DIRECTION('ref_axis',(1.,0.,0.));
#9563=DIRECTION('',(0.,1.,0.));
#9564=DIRECTION('center_axis',(0.,0.,1.));
#9565=DIRECTION('ref_axis',(1.,0.,0.));
#9566=DIRECTION('center_axis',(0.,0.,1.));
#9567=DIRECTION('ref_axis',(1.,0.,0.));
#9568=DIRECTION('center_axis',(0.,0.,1.));
#9569=DIRECTION('ref_axis',(1.,0.,0.));
#9570=DIRECTION('center_axis',(0.,0.,1.));
#9571=DIRECTION('ref_axis',(1.,0.,0.));
#9572=DIRECTION('',(0.,0.,1.));
#9573=DIRECTION('center_axis',(-0.871575537124549,0.,-0.490261239632559));
#9574=DIRECTION('ref_axis',(0.490261239632559,0.,-0.871575537124549));
#9575=DIRECTION('center_axis',(0.,0.,1.));
#9576=DIRECTION('ref_axis',(1.,0.,0.));
#9577=DIRECTION('center_axis',(0.,0.,1.));
#9578=DIRECTION('ref_axis',(1.,0.,0.));
#9579=DIRECTION('center_axis',(0.,0.,1.));
#9580=DIRECTION('ref_axis',(1.,0.,0.));
#9581=DIRECTION('center_axis',(0.,0.,1.));
#9582=DIRECTION('ref_axis',(1.,0.,0.));
#9583=DIRECTION('',(0.,0.,1.));
#9584=DIRECTION('center_axis',(0.,0.,1.));
#9585=DIRECTION('ref_axis',(1.,0.,0.));
#9586=DIRECTION('center_axis',(0.,0.,1.));
#9587=DIRECTION('ref_axis',(1.,0.,0.));
#9588=DIRECTION('',(0.,0.,1.));
#9589=DIRECTION('center_axis',(0.871575537124549,0.,0.490261239632559));
#9590=DIRECTION('ref_axis',(0.490261239632559,0.,-0.871575537124549));
#9591=DIRECTION('',(0.,1.,0.));
#9592=DIRECTION('',(-0.490261239632559,0.,0.871575537124549));
#9593=DIRECTION('',(0.,1.,0.));
#9594=DIRECTION('',(0.490261239632559,0.,-0.871575537124549));
#9595=DIRECTION('center_axis',(-0.871575537124549,0.,0.490261239632559));
#9596=DIRECTION('ref_axis',(0.490261239632559,0.,0.871575537124549));
#9597=DIRECTION('',(0.,-1.,0.));
#9598=DIRECTION('',(0.490261239632559,0.,0.871575537124549));
#9599=DIRECTION('',(0.,1.,0.));
#9600=DIRECTION('',(-0.490261239632559,0.,-0.871575537124549));
#9601=DIRECTION('center_axis',(-1.,0.,0.));
#9602=DIRECTION('ref_axis',(0.,0.,1.));
#9603=DIRECTION('',(0.,0.,-1.));
#9604=DIRECTION('',(0.,0.,1.));
#9605=DIRECTION('',(0.,1.,0.));
#9606=DIRECTION('center_axis',(0.,0.,-1.));
#9607=DIRECTION('ref_axis',(-1.,0.,0.));
#9608=DIRECTION('',(1.,0.,0.));
#9609=DIRECTION('',(-1.,0.,0.));
#9610=DIRECTION('',(0.,1.,0.));
#9611=DIRECTION('center_axis',(1.,0.,0.));
#9612=DIRECTION('ref_axis',(0.,0.,-1.));
#9613=DIRECTION('',(0.,0.,1.));
#9614=DIRECTION('',(0.,0.,-1.));
#9615=DIRECTION('center_axis',(0.,1.,0.));
#9616=DIRECTION('ref_axis',(1.,0.,0.));
#9617=DIRECTION('center_axis',(0.,1.,0.));
#9618=DIRECTION('ref_axis',(1.,0.,0.));
#9619=DIRECTION('center_axis',(0.,-1.,0.));
#9620=DIRECTION('ref_axis',(1.,0.,0.));
#9621=DIRECTION('center_axis',(0.,1.,0.));
#9622=DIRECTION('ref_axis',(1.,0.,0.));
#9623=DIRECTION('',(0.,-1.,0.));
#9624=DIRECTION('center_axis',(0.,-1.,0.));
#9625=DIRECTION('ref_axis',(1.,0.,0.));
#9626=DIRECTION('center_axis',(0.,1.,0.));
#9627=DIRECTION('ref_axis',(6.12323399573677E-17,0.,1.));
#9628=DIRECTION('center_axis',(0.,1.,0.));
#9629=DIRECTION('ref_axis',(1.,0.,0.));
#9630=DIRECTION('center_axis',(0.,1.,0.));
#9631=DIRECTION('ref_axis',(1.,0.,0.));
#11958=CARTESIAN_POINT('',(0.,0.,0.));
#11959=CARTESIAN_POINT('Origin',(-2.,6.1,7.));
#11960=CARTESIAN_POINT('',(-2.165,6.2,7.));
#11961=CARTESIAN_POINT('Origin',(-2.,6.2,7.));
#11962=CARTESIAN_POINT('',(-2.165,7.8,7.));
#11963=CARTESIAN_POINT('',(-2.165,6.1,7.));
#11964=CARTESIAN_POINT('Origin',(-2.,7.8,7.));
#11965=CARTESIAN_POINT('Origin',(1.22464679914735E-16,6.1,9.));
#11966=CARTESIAN_POINT('',(-0.165,6.2,9.));
#11967=CARTESIAN_POINT('Origin',(1.22464679914735E-16,6.2,9.));
#11968=CARTESIAN_POINT('',(-0.165,7.8,9.));
#11969=CARTESIAN_POINT('',(-0.165,6.1,9.));
#11970=CARTESIAN_POINT('Origin',(1.22464679914735E-16,7.8,9.));
#11971=CARTESIAN_POINT('Origin',(2.,6.1,7.));
#11972=CARTESIAN_POINT('',(1.835,6.2,7.));
#11973=CARTESIAN_POINT('Origin',(2.,6.2,7.));
#11974=CARTESIAN_POINT('',(1.835,7.8,7.));
#11975=CARTESIAN_POINT('',(1.835,6.1,7.));
#11976=CARTESIAN_POINT('Origin',(2.,7.8,7.));
#11977=CARTESIAN_POINT('Origin',(-3.67394039744206E-16,6.1,5.));
#11978=CARTESIAN_POINT('',(-0.165,6.2,5.));
#11979=CARTESIAN_POINT('Origin',(-3.67394039744206E-16,6.2,5.));
#11980=CARTESIAN_POINT('',(-0.165,7.8,5.));
#11981=CARTESIAN_POINT('',(-0.165,6.1,5.));
#11982=CARTESIAN_POINT('Origin',(-3.67394039744206E-16,7.8,5.));
#11983=CARTESIAN_POINT('Origin',(-2.7,7.,4.3));
#11984=CARTESIAN_POINT('',(-2.20625,7.34089725358237,4.3));
#11985=CARTESIAN_POINT('',(-2.20625,6.65910274641763,4.3));
#11986=CARTESIAN_POINT('',(-2.20625,6.6,4.3));
#11987=CARTESIAN_POINT('Origin',(-2.7,7.,4.3));
#11988=CARTESIAN_POINT('Origin',(-2.7,7.,1.8));
#11989=CARTESIAN_POINT('',(-3.3,7.,1.8));
#11990=CARTESIAN_POINT('Origin',(-2.7,7.,1.8));
#11991=CARTESIAN_POINT('',(-3.3,7.,2.35555555555556));
#11992=CARTESIAN_POINT('',(-3.3,7.,1.8));
#11993=CARTESIAN_POINT('Origin',(-2.7,7.,3.42222222222222));
#11994=CARTESIAN_POINT('Origin',(-2.7,7.,3.42222222222222));
#11995=CARTESIAN_POINT('Origin',(-2.7,7.,1.8));
#11996=CARTESIAN_POINT('',(-3.03,7.,1.8));
#11997=CARTESIAN_POINT('Origin',(-2.7,7.,1.8));
#11998=CARTESIAN_POINT('Origin',(2.7,7.,4.3));
#11999=CARTESIAN_POINT('',(2.20625,6.65910274641764,4.3));
#12000=CARTESIAN_POINT('',(2.20625,7.34089725358236,4.3));
#12001=CARTESIAN_POINT('',(2.20625,6.6,4.3));
#12002=CARTESIAN_POINT('',(2.1,7.,4.3));
#12003=CARTESIAN_POINT('Origin',(2.7,7.,4.3));
#12004=CARTESIAN_POINT('Origin',(2.7,7.,4.3));
#12005=CARTESIAN_POINT('Origin',(2.7,7.,1.8));
#12006=CARTESIAN_POINT('',(2.1,7.,1.8));
#12007=CARTESIAN_POINT('Origin',(2.7,7.,1.8));
#12008=CARTESIAN_POINT('',(2.1,7.,1.8));
#12009=CARTESIAN_POINT('Origin',(2.7,7.,3.42222222222222));
#12010=CARTESIAN_POINT('Origin',(2.7,7.,1.8));
#12011=CARTESIAN_POINT('',(2.37,7.,1.8));
#12012=CARTESIAN_POINT('Origin',(2.7,7.,1.8));
#12013=CARTESIAN_POINT('Origin',(-2.7,7.,0.9));
#12014=CARTESIAN_POINT('',(-3.03,7.,1.));
#12015=CARTESIAN_POINT('Origin',(-2.7,7.,1.));
#12016=CARTESIAN_POINT('',(-3.03,7.,0.9));
#12017=CARTESIAN_POINT('Origin',(2.7,7.,0.9));
#12018=CARTESIAN_POINT('',(2.37,7.,1.));
#12019=CARTESIAN_POINT('Origin',(2.7,7.,1.));
#12020=CARTESIAN_POINT('',(2.37,7.,0.9));
#12021=CARTESIAN_POINT('Origin',(1.7,6.2,5.2));
#12022=CARTESIAN_POINT('',(1.71218189678592,6.2,5.17834329460281));
#12023=CARTESIAN_POINT('',(1.71218189678592,7.8,5.17834329460281));
#12024=CARTESIAN_POINT('',(1.71218189678592,6.2,5.17834329460281));
#12025=CARTESIAN_POINT('',(3.5,6.2,2.));
#12026=CARTESIAN_POINT('',(3.5,6.2,2.));
#12027=CARTESIAN_POINT('',(3.5,7.8,2.));
#12028=CARTESIAN_POINT('',(3.5,6.2,2.));
#12029=CARTESIAN_POINT('',(3.5,7.8,2.));
#12030=CARTESIAN_POINT('Origin',(-3.5,6.2,2.));
#12031=CARTESIAN_POINT('',(-1.71218189678592,7.8,5.17834329460281));
#12032=CARTESIAN_POINT('',(-1.71218189678592,6.2,5.17834329460281));
#12033=CARTESIAN_POINT('',(-1.71218189678592,6.2,5.17834329460281));
#12034=CARTESIAN_POINT('',(-3.5,7.8,2.));
#12035=CARTESIAN_POINT('',(-1.7,7.8,5.2));
#12036=CARTESIAN_POINT('',(-3.5,6.2,2.));
#12037=CARTESIAN_POINT('',(-3.5,6.2,2.));
#12038=CARTESIAN_POINT('',(-1.7,6.2,5.2));
#12039=CARTESIAN_POINT('Origin',(-3.5,6.2,1.));
#12040=CARTESIAN_POINT('',(-3.5,6.2,1.));
#12041=CARTESIAN_POINT('',(-3.5,6.2,2.));
#12042=CARTESIAN_POINT('',(-3.5,7.8,1.));
#12043=CARTESIAN_POINT('',(-3.5,7.8,2.));
#12044=CARTESIAN_POINT('',(-3.5,6.2,1.));
#12045=CARTESIAN_POINT('Origin',(3.5,6.2,1.));
#12046=CARTESIAN_POINT('',(3.5,6.2,1.));
#12047=CARTESIAN_POINT('',(-3.5,6.2,1.));
#12048=CARTESIAN_POINT('',(3.5,7.8,1.));
#12049=CARTESIAN_POINT('',(-3.5,7.8,1.));
#12050=CARTESIAN_POINT('',(3.5,6.2,1.));
#12051=CARTESIAN_POINT('Origin',(3.5,6.2,2.));
#12052=CARTESIAN_POINT('',(3.5,6.2,1.));
#12053=CARTESIAN_POINT('',(3.5,7.8,1.));
#12054=CARTESIAN_POINT('Origin',(0.,7.8,7.));
#12055=CARTESIAN_POINT('Origin',(0.,7.8,7.));
#12056=CARTESIAN_POINT('',(-1.6,7.8,7.));
#12057=CARTESIAN_POINT('Origin',(0.,7.8,7.));
#12058=CARTESIAN_POINT('Origin',(0.,6.2,7.));
#12059=CARTESIAN_POINT('',(-1.6,6.2,7.));
#12060=CARTESIAN_POINT('',(-1.6,6.2,7.));
#12061=CARTESIAN_POINT('Origin',(0.,6.2,7.));
#12062=CARTESIAN_POINT('Origin',(0.,6.2,7.));
#12063=CARTESIAN_POINT('Origin',(0.,6.2,7.));
#12064=CARTESIAN_POINT('Origin',(0.,6.2,7.));
#14739=UNCERTAINTY_MEASURE_WITH_UNIT(LENGTH_MEASURE(0.001),#14823,
'DISTANCE_ACCURACY_VALUE',
'Maximum model space distance between geometric entities at asserted c
onnectivities');
#14777=UNCERTAINTY_MEASURE_WITH_UNIT(LENGTH_MEASURE(0.001),#14823,
'DISTANCE_ACCURACY_VALUE',
'Maximum model space distance between geometric entities at asserted c
onnectivities');
#14784=(
GEOMETRIC_REPRESENTATION_CONTEXT(3)
GLOBAL_UNCERTAINTY_ASSIGNED_CONTEXT((#14739))
GLOBAL_UNIT_ASSIGNED_CONTEXT((#14823,#14825,#14826))
REPRESENTATION_CONTEXT('','3D')
);
#14822=(
GEOMETRIC_REPRESENTATION_CONTEXT(3)
GLOBAL_UNCERTAINTY_ASSIGNED_CONTEXT((#14777))
GLOBAL_UNIT_ASSIGNED_CONTEXT((#14823,#14825,#14826))
REPRESENTATION_CONTEXT('','3D')
);
#14823=(
LENGTH_UNIT()
NAMED_UNIT(*)
SI_UNIT(.CENTI.,.METRE.)
);
#14825=(
NAMED_UNIT(*)
PLANE_ANGLE_UNIT()
SI_UNIT($,.RADIAN.)
);
#14826=(
NAMED_UNIT(*)
SI_UNIT($,.STERADIAN.)
SOLID_ANGLE_UNIT()
);
#14833=SHAPE_DEFINITION_REPRESENTATION(#14877,#15004);
#14877=PRODUCT_DEFINITION_SHAPE('',$,#15049);
#15004=SHAPE_REPRESENTATION('',(#8283),#14784);
#15042=PRODUCT_DEFINITION_CONTEXT('part definition',#15176,'design');
#15049=PRODUCT_DEFINITION('Support housing (1)','Support housing (1)',#15093,
#15042);
#15093=PRODUCT_DEFINITION_FORMATION('',$,#15184);
#15176=APPLICATION_CONTEXT(
'Core Data for Automotive Mechanical Design Process');
#15177=PRODUCT_CONTEXT('part definition',#15176,'mechanical');
#15184=PRODUCT('Support housing (1)','Support housing (1)',
'Support housing (1)',(#15177));
#15257=COLOUR_RGB('Dark Blue',0.08,0.2,0.34);
#15258=FILL_AREA_STYLE_COLOUR('',#15257);
#15259=FILL_AREA_STYLE('',(#15258));
#15260=SURFACE_STYLE_FILL_AREA(#15259);
#15261=SURFACE_SIDE_STYLE('',(#15260));
#15262=SURFACE_STYLE_USAGE(.BOTH.,#15261);
#15263=PRESENTATION_STYLE_ASSIGNMENT((#15262));
ENDSEC;
END-ISO-10303-21;
